ISO-10303-21;
HEADER;
/* Generated by software containing ST-Developer
 * from STEP Tools, Inc. (www.steptools.com) 
 */

FILE_DESCRIPTION(
/* description */ ('PAT-091'),
/* implementation_level */ '2;1');

FILE_NAME(
/* name */ 'Plain pivot bush (3).step',
/* time_stamp */ '2026-10-27T15:34:44-07:00',
/* author */ (''),
/* organization */ (''),
/* preprocessor_version */ 'ST-DEVELOPER v20.2',
/* originating_system */ 'Autodesk Translation Framework v15.17.0.0',
/* authorisation */ '');

FILE_SCHEMA (('AUTOMOTIVE_DESIGN { 1 0 10303 214 3 1 1 }'));
ENDSEC;

DATA;
#10=MECHANICAL_DESIGN_GEOMETRIC_PRESENTATION_REPRESENTATION('',(#1032),#25100);
#812=SHAPE_REPRESENTATION_RELATIONSHIP('SRR','None',#25578,#922);
#922=ADVANCED_BREP_SHAPE_REPRESENTATION('',(#1154),#25048);
#1032=STYLED_ITEM('',(#26177),#1154);
#1154=MANIFOLD_SOLID_BREP('Body1',#13311);
#1502=FACE_BOUND('',#3657,.T.);
#1503=FACE_BOUND('',#3659,.T.);
#1913=PLANE('',#15576);
#1914=PLANE('',#15577);
#2549=FACE_OUTER_BOUND('',#3654,.T.);
#2550=FACE_OUTER_BOUND('',#3655,.T.);
#2551=FACE_OUTER_BOUND('',#3656,.T.);
#2552=FACE_OUTER_BOUND('',#3658,.T.);
#3654=EDGE_LOOP('',(#10942,#10943,#10944,#10945));
#3655=EDGE_LOOP('',(#10946,#10947,#10948,#10949));
#3656=EDGE_LOOP('',(#10950));
#3657=EDGE_LOOP('',(#10951));
#3658=EDGE_LOOP('',(#10952));
#3659=EDGE_LOOP('',(#10953));
#4677=LINE('',#23226,#5417);
#4678=LINE('',#23232,#5418);
#5417=VECTOR('',#18995,0.605);
#5418=VECTOR('',#19002,1.);
#6032=CIRCLE('',#15571,0.605);
#6033=CIRCLE('',#15572,0.605);
#6034=CIRCLE('',#15574,1.);
#6035=CIRCLE('',#15575,1.);
#7037=VERTEX_POINT('',#23223);
#7038=VERTEX_POINT('',#23225);
#7039=VERTEX_POINT('',#23229);
#7040=VERTEX_POINT('',#23231);
#8406=EDGE_CURVE('',#7037,#7037,#6032,.T.);
#8407=EDGE_CURVE('',#7037,#7038,#4677,.T.);
#8408=EDGE_CURVE('',#7038,#7038,#6033,.T.);
#8409=EDGE_CURVE('',#7039,#7039,#6034,.T.);
#8410=EDGE_CURVE('',#7039,#7040,#4678,.T.);
#8411=EDGE_CURVE('',#7040,#7040,#6035,.T.);
#10942=ORIENTED_EDGE('',*,*,#8406,.F.);
#10943=ORIENTED_EDGE('',*,*,#8407,.T.);
#10944=ORIENTED_EDGE('',*,*,#8408,.T.);
#10945=ORIENTED_EDGE('',*,*,#8407,.F.);
#10946=ORIENTED_EDGE('',*,*,#8409,.F.);
#10947=ORIENTED_EDGE('',*,*,#8410,.T.);
#10948=ORIENTED_EDGE('',*,*,#8411,.T.);
#10949=ORIENTED_EDGE('',*,*,#8410,.F.);
#10950=ORIENTED_EDGE('',*,*,#8409,.T.);
#10951=ORIENTED_EDGE('',*,*,#8406,.T.);
#10952=ORIENTED_EDGE('',*,*,#8411,.F.);
#10953=ORIENTED_EDGE('',*,*,#8408,.F.);
#12279=CYLINDRICAL_SURFACE('',#15570,0.605);
#12280=CYLINDRICAL_SURFACE('',#15573,1.);
#12916=ADVANCED_FACE('',(#2549),#12279,.F.);
#12917=ADVANCED_FACE('',(#2550),#12280,.T.);
#12918=ADVANCED_FACE('',(#2551,#1502),#1913,.T.);
#12919=ADVANCED_FACE('',(#2552,#1503),#1914,.F.);
#13311=CLOSED_SHELL('',(#12916,#12917,#12918,#12919));
#15569=AXIS2_PLACEMENT_3D('',#23221,#18989,#18990);
#15570=AXIS2_PLACEMENT_3D('',#23222,#18991,#18992);
#15571=AXIS2_PLACEMENT_3D('',#23224,#18993,#18994);
#15572=AXIS2_PLACEMENT_3D('',#23227,#18996,#18997);
#15573=AXIS2_PLACEMENT_3D('',#23228,#18998,#18999);
#15574=AXIS2_PLACEMENT_3D('',#23230,#19000,#19001);
#15575=AXIS2_PLACEMENT_3D('',#23233,#19003,#19004);
#15576=AXIS2_PLACEMENT_3D('',#23234,#19005,#19006);
#15577=AXIS2_PLACEMENT_3D('',#23235,#19007,#19008);
#18989=DIRECTION('axis',(0.,0.,1.));
#18990=DIRECTION('refdir',(1.,0.,0.));
#18991=DIRECTION('center_axis',(0.,1.,0.));
#18992=DIRECTION('ref_axis',(1.,0.,0.));
#18993=DIRECTION('center_axis',(0.,-1.,0.));
#18994=DIRECTION('ref_axis',(1.,0.,0.));
#18995=DIRECTION('',(0.,-1.,0.));
#18996=DIRECTION('center_axis',(0.,-1.,0.));
#18997=DIRECTION('ref_axis',(1.,0.,0.));
#18998=DIRECTION('center_axis',(0.,1.,0.));
#18999=DIRECTION('ref_axis',(1.,0.,0.));
#19000=DIRECTION('center_axis',(0.,1.,0.));
#19001=DIRECTION('ref_axis',(1.,0.,0.));
#19002=DIRECTION('',(0.,-1.,0.));
#19003=DIRECTION('center_axis',(0.,1.,0.));
#19004=DIRECTION('ref_axis',(1.,0.,0.));
#19005=DIRECTION('center_axis',(0.,1.,0.));
#19006=DIRECTION('ref_axis',(1.,0.,0.));
#19007=DIRECTION('center_axis',(0.,1.,0.));
#19008=DIRECTION('ref_axis',(1.,0.,0.));
#23221=CARTESIAN_POINT('',(0.,0.,0.));
#23222=CARTESIAN_POINT('Origin',(0.,5.,3.));
#23223=CARTESIAN_POINT('',(-0.605,6.,3.));
#23224=CARTESIAN_POINT('Origin',(0.,6.,3.));
#23225=CARTESIAN_POINT('',(-0.605,5.,3.));
#23226=CARTESIAN_POINT('',(-0.605,5.,3.));
#23227=CARTESIAN_POINT('Origin',(0.,5.,3.));
#23228=CARTESIAN_POINT('Origin',(0.,5.,3.));
#23229=CARTESIAN_POINT('',(-1.,6.,3.));
#23230=CARTESIAN_POINT('Origin',(0.,6.,3.));
#23231=CARTESIAN_POINT('',(-1.,5.,3.));
#23232=CARTESIAN_POINT('',(-1.,5.,3.));
#23233=CARTESIAN_POINT('Origin',(0.,5.,3.));
#23234=CARTESIAN_POINT('Origin',(0.,6.,3.));
#23235=CARTESIAN_POINT('Origin',(0.,5.,3.));
#24927=UNCERTAINTY_MEASURE_WITH_UNIT(LENGTH_MEASURE(0.001),#25101,
'DISTANCE_ACCURACY_VALUE',
'Maximum model space distance between geometric entities at asserted c
onnectivities');
#24979=UNCERTAINTY_MEASURE_WITH_UNIT(LENGTH_MEASURE(0.001),#25101,
'DISTANCE_ACCURACY_VALUE',
'Maximum model space distance between geometric entities at asserted c
onnectivities');
#25048=(
GEOMETRIC_REPRESENTATION_CONTEXT(3)
GLOBAL_UNCERTAINTY_ASSIGNED_CONTEXT((#24927))
GLOBAL_UNIT_ASSIGNED_CONTEXT((#25101,#25103,#25104))
REPRESENTATION_CONTEXT('','3D')
);
#25100=(
GEOMETRIC_REPRESENTATION_CONTEXT(3)
GLOBAL_UNCERTAINTY_ASSIGNED_CONTEXT((#24979))
GLOBAL_UNIT_ASSIGNED_CONTEXT((#25101,#25103,#25104))
REPRESENTATION_CONTEXT('','3D')
);
#25101=(
LENGTH_UNIT()
NAMED_UNIT(*)
SI_UNIT(.CENTI.,.METRE.)
);
#25103=(
NAMED_UNIT(*)
PLANE_ANGLE_UNIT()
SI_UNIT($,.RADIAN.)
);
#25104=(
NAMED_UNIT(*)
SI_UNIT($,.STERADIAN.)
SOLID_ANGLE_UNIT()
);
#25173=SHAPE_DEFINITION_REPRESENTATION(#25295,#25578);
#25295=PRODUCT_DEFINITION_SHAPE('',$,#25699);
#25578=SHAPE_REPRESENTATION('',(#15569),#25048);
#25630=PRODUCT_DEFINITION_CONTEXT('part definition',#25992,'design');
#25699=PRODUCT_DEFINITION('Plain pivot bush (3)','Plain pivot bush (3)',#25819,
#25630);
#25819=PRODUCT_DEFINITION_FORMATION('',$,#26062);
#25992=APPLICATION_CONTEXT(
'Core Data for Automotive Mechanical Design Process');
#25993=PRODUCT_CONTEXT('part definition',#25992,'mechanical');
#26062=PRODUCT('Plain pivot bush (3)','Plain pivot bush (3)',
'Plain pivot bush (3)',(#25993));
#26171=COLOUR_RGB('Light Blue',0.38,0.62,0.78);
#26172=FILL_AREA_STYLE_COLOUR('',#26171);
#26173=FILL_AREA_STYLE('',(#26172));
#26174=SURFACE_STYLE_FILL_AREA(#26173);
#26175=SURFACE_SIDE_STYLE('',(#26174));
#26176=SURFACE_STYLE_USAGE(.BOTH.,#26175);
#26177=PRESENTATION_STYLE_ASSIGNMENT((#26176));
ENDSEC;
END-ISO-10303-21;
